ISO-10303-21;
HEADER;
/* Generated by software containing ST-Developer
 * from STEP Tools, Inc. (www.steptools.com) 
 */

FILE_DESCRIPTION(
/* description */ (''),
/* implementation_level */ '2;1');

FILE_NAME(
/* name */ 'Screw_03.step',
/* time_stamp */ '2026-10-04T23:23:09-07:00',
/* author */ (''),
/* organization */ (''),
/* preprocessor_version */ 'ST-DEVELOPER v20.2',
/* originating_system */ 'Autodesk Translation Framework v15.15.0.0',
/* authorisation */ '');

FILE_SCHEMA (('AUTOMOTIVE_DESIGN { 1 0 10303 214 3 1 1 }'));
ENDSEC;

DATA;
#10=MECHANICAL_DESIGN_GEOMETRIC_PRESENTATION_REPRESENTATION('',(#70,#71),#2676);
#45=SPHERICAL_SURFACE('',#1703,1.);
#52=SHAPE_REPRESENTATION_RELATIONSHIP('SRR','None',#2711,#60);
#60=ADVANCED_BREP_SHAPE_REPRESENTATION('',(#81,#82),#2671);
#70=STYLED_ITEM('',(#2757),#81);
#71=STYLED_ITEM('',(#2757),#82);
#81=MANIFOLD_SOLID_BREP('Body1',#1481);
#82=MANIFOLD_SOLID_BREP('Body1',#1482);
#101=CYLINDRICAL_SURFACE('',#1676,1.);
#102=CYLINDRICAL_SURFACE('',#1680,2.);
#103=CYLINDRICAL_SURFACE('',#1688,1.);
#104=CYLINDRICAL_SURFACE('',#1692,1.);
#105=CYLINDRICAL_SURFACE('',#1696,2.);
#124=FACE_BOUND('',#350,.T.);
#125=FACE_BOUND('',#355,.T.);
#126=FACE_BOUND('',#358,.T.);
#127=FACE_BOUND('',#363,.T.);
#128=FACE_BOUND('',#367,.T.);
#157=PLANE('',#1673);
#158=PLANE('',#1682);
#159=PLANE('',#1685);
#160=PLANE('',#1690);
#161=PLANE('',#1694);
#162=PLANE('',#1700);
#236=FACE_OUTER_BOUND('',#349,.T.);
#237=FACE_OUTER_BOUND('',#351,.T.);
#238=FACE_OUTER_BOUND('',#352,.T.);
#239=FACE_OUTER_BOUND('',#353,.T.);
#240=FACE_OUTER_BOUND('',#354,.T.);
#241=FACE_OUTER_BOUND('',#356,.T.);
#242=FACE_OUTER_BOUND('',#357,.T.);
#243=FACE_OUTER_BOUND('',#359,.T.);
#244=FACE_OUTER_BOUND('',#360,.T.);
#245=FACE_OUTER_BOUND('',#361,.T.);
#246=FACE_OUTER_BOUND('',#362,.T.);
#247=FACE_OUTER_BOUND('',#364,.T.);
#248=FACE_OUTER_BOUND('',#365,.T.);
#249=FACE_OUTER_BOUND('',#366,.T.);
#250=FACE_OUTER_BOUND('',#368,.T.);
#251=FACE_OUTER_BOUND('',#369,.T.);
#349=EDGE_LOOP('',(#1164));
#350=EDGE_LOOP('',(#1165));
#351=EDGE_LOOP('',(#1166,#1167,#1168,#1169));
#352=EDGE_LOOP('',(#1170,#1171,#1172,#1173));
#353=EDGE_LOOP('',(#1174,#1175,#1176,#1177));
#354=EDGE_LOOP('',(#1178));
#355=EDGE_LOOP('',(#1179));
#356=EDGE_LOOP('',(#1180,#1181,#1182,#1183));
#357=EDGE_LOOP('',(#1184));
#358=EDGE_LOOP('',(#1185));
#359=EDGE_LOOP('',(#1186,#1187,#1188,#1189));
#360=EDGE_LOOP('',(#1190));
#361=EDGE_LOOP('',(#1191,#1192,#1193,#1194));
#362=EDGE_LOOP('',(#1195));
#363=EDGE_LOOP('',(#1196));
#364=EDGE_LOOP('',(#1197,#1198,#1199,#1200));
#365=EDGE_LOOP('',(#1201,#1202,#1203,#1204));
#366=EDGE_LOOP('',(#1205));
#367=EDGE_LOOP('',(#1206));
#368=EDGE_LOOP('',(#1207,#1208,#1209,#1210));
#369=EDGE_LOOP('',(#1211,#1212,#1213));
#449=LINE('',#2442,#559);
#450=LINE('',#2445,#560);
#451=LINE('',#2449,#561);
#452=LINE('',#2455,#562);
#453=LINE('',#2463,#563);
#454=LINE('',#2471,#564);
#455=LINE('',#2478,#565);
#456=LINE('',#2481,#566);
#457=LINE('',#2487,#567);
#559=VECTOR('',#2006,1.);
#560=VECTOR('',#2009,1.1);
#561=VECTOR('',#2014,2.);
#562=VECTOR('',#2023,1.9);
#563=VECTOR('',#2032,1.);
#564=VECTOR('',#2043,1.);
#565=VECTOR('',#2052,2.);
#566=VECTOR('',#2055,1.9);
#567=VECTOR('',#2064,1.1);
#672=CIRCLE('',#1674,2.);
#673=CIRCLE('',#1675,1.);
#674=CIRCLE('',#1677,1.);
#675=CIRCLE('',#1679,1.2);
#676=CIRCLE('',#1681,2.);
#677=CIRCLE('',#1683,1.8);
#678=CIRCLE('',#1686,1.);
#679=CIRCLE('',#1687,0.866025403784439);
#680=CIRCLE('',#1689,1.);
#681=CIRCLE('',#1691,1.);
#682=CIRCLE('',#1693,1.);
#683=CIRCLE('',#1695,2.);
#684=CIRCLE('',#1697,2.);
#685=CIRCLE('',#1699,1.8);
#686=CIRCLE('',#1701,1.2);
#687=CIRCLE('',#1704,1.);
#753=VERTEX_POINT('',#2435);
#754=VERTEX_POINT('',#2437);
#755=VERTEX_POINT('',#2440);
#756=VERTEX_POINT('',#2444);
#757=VERTEX_POINT('',#2448);
#758=VERTEX_POINT('',#2452);
#759=VERTEX_POINT('',#2457);
#760=VERTEX_POINT('',#2459);
#761=VERTEX_POINT('',#2462);
#762=VERTEX_POINT('',#2466);
#763=VERTEX_POINT('',#2469);
#764=VERTEX_POINT('',#2473);
#765=VERTEX_POINT('',#2476);
#766=VERTEX_POINT('',#2480);
#767=VERTEX_POINT('',#2484);
#768=VERTEX_POINT('',#2489);
#900=EDGE_CURVE('',#753,#753,#672,.T.);
#901=EDGE_CURVE('',#754,#754,#673,.T.);
#902=EDGE_CURVE('',#755,#755,#674,.T.);
#903=EDGE_CURVE('',#755,#754,#449,.T.);
#904=EDGE_CURVE('',#755,#756,#450,.T.);
#905=EDGE_CURVE('',#756,#756,#675,.T.);
#906=EDGE_CURVE('',#753,#757,#451,.T.);
#907=EDGE_CURVE('',#757,#757,#676,.T.);
#908=EDGE_CURVE('',#758,#758,#677,.T.);
#909=EDGE_CURVE('',#757,#758,#452,.T.);
#910=EDGE_CURVE('',#759,#759,#678,.T.);
#911=EDGE_CURVE('',#760,#760,#679,.T.);
#912=EDGE_CURVE('',#759,#761,#453,.T.);
#913=EDGE_CURVE('',#761,#761,#680,.T.);
#914=EDGE_CURVE('',#762,#762,#681,.T.);
#915=EDGE_CURVE('',#763,#763,#682,.T.);
#916=EDGE_CURVE('',#763,#762,#454,.T.);
#917=EDGE_CURVE('',#764,#764,#683,.T.);
#918=EDGE_CURVE('',#765,#765,#684,.T.);
#919=EDGE_CURVE('',#765,#764,#455,.T.);
#920=EDGE_CURVE('',#765,#766,#456,.T.);
#921=EDGE_CURVE('',#766,#766,#685,.T.);
#922=EDGE_CURVE('',#767,#767,#686,.T.);
#923=EDGE_CURVE('',#761,#767,#457,.T.);
#924=EDGE_CURVE('',#760,#768,#687,.T.);
#1164=ORIENTED_EDGE('',*,*,#900,.T.);
#1165=ORIENTED_EDGE('',*,*,#901,.T.);
#1166=ORIENTED_EDGE('',*,*,#902,.F.);
#1167=ORIENTED_EDGE('',*,*,#903,.T.);
#1168=ORIENTED_EDGE('',*,*,#901,.F.);
#1169=ORIENTED_EDGE('',*,*,#903,.F.);
#1170=ORIENTED_EDGE('',*,*,#902,.T.);
#1171=ORIENTED_EDGE('',*,*,#904,.T.);
#1172=ORIENTED_EDGE('',*,*,#905,.T.);
#1173=ORIENTED_EDGE('',*,*,#904,.F.);
#1174=ORIENTED_EDGE('',*,*,#900,.F.);
#1175=ORIENTED_EDGE('',*,*,#906,.T.);
#1176=ORIENTED_EDGE('',*,*,#907,.F.);
#1177=ORIENTED_EDGE('',*,*,#906,.F.);
#1178=ORIENTED_EDGE('',*,*,#908,.F.);
#1179=ORIENTED_EDGE('',*,*,#905,.F.);
#1180=ORIENTED_EDGE('',*,*,#907,.T.);
#1181=ORIENTED_EDGE('',*,*,#909,.T.);
#1182=ORIENTED_EDGE('',*,*,#908,.T.);
#1183=ORIENTED_EDGE('',*,*,#909,.F.);
#1184=ORIENTED_EDGE('',*,*,#910,.T.);
#1185=ORIENTED_EDGE('',*,*,#911,.T.);
#1186=ORIENTED_EDGE('',*,*,#910,.F.);
#1187=ORIENTED_EDGE('',*,*,#912,.T.);
#1188=ORIENTED_EDGE('',*,*,#913,.T.);
#1189=ORIENTED_EDGE('',*,*,#912,.F.);
#1190=ORIENTED_EDGE('',*,*,#914,.T.);
#1191=ORIENTED_EDGE('',*,*,#915,.T.);
#1192=ORIENTED_EDGE('',*,*,#916,.T.);
#1193=ORIENTED_EDGE('',*,*,#914,.F.);
#1194=ORIENTED_EDGE('',*,*,#916,.F.);
#1195=ORIENTED_EDGE('',*,*,#917,.F.);
#1196=ORIENTED_EDGE('',*,*,#915,.F.);
#1197=ORIENTED_EDGE('',*,*,#918,.F.);
#1198=ORIENTED_EDGE('',*,*,#919,.T.);
#1199=ORIENTED_EDGE('',*,*,#917,.T.);
#1200=ORIENTED_EDGE('',*,*,#919,.F.);
#1201=ORIENTED_EDGE('',*,*,#918,.T.);
#1202=ORIENTED_EDGE('',*,*,#920,.T.);
#1203=ORIENTED_EDGE('',*,*,#921,.T.);
#1204=ORIENTED_EDGE('',*,*,#920,.F.);
#1205=ORIENTED_EDGE('',*,*,#921,.F.);
#1206=ORIENTED_EDGE('',*,*,#922,.F.);
#1207=ORIENTED_EDGE('',*,*,#913,.F.);
#1208=ORIENTED_EDGE('',*,*,#923,.T.);
#1209=ORIENTED_EDGE('',*,*,#922,.T.);
#1210=ORIENTED_EDGE('',*,*,#923,.F.);
#1211=ORIENTED_EDGE('',*,*,#911,.F.);
#1212=ORIENTED_EDGE('',*,*,#924,.T.);
#1213=ORIENTED_EDGE('',*,*,#924,.F.);
#1371=CONICAL_SURFACE('',#1678,1.1,0.785398163397448);
#1372=CONICAL_SURFACE('',#1684,1.9,0.785398163397448);
#1373=CONICAL_SURFACE('',#1698,1.9,0.785398163397448);
#1374=CONICAL_SURFACE('',#1702,1.1,0.785398163397448);
#1427=ADVANCED_FACE('',(#236,#124),#157,.F.);
#1428=ADVANCED_FACE('',(#237),#101,.F.);
#1429=ADVANCED_FACE('',(#238),#1371,.F.);
#1430=ADVANCED_FACE('',(#239),#102,.T.);
#1431=ADVANCED_FACE('',(#240,#125),#158,.T.);
#1432=ADVANCED_FACE('',(#241),#1372,.T.);
#1433=ADVANCED_FACE('',(#242,#126),#159,.F.);
#1434=ADVANCED_FACE('',(#243),#103,.T.);
#1435=ADVANCED_FACE('',(#244),#160,.T.);
#1436=ADVANCED_FACE('',(#245),#104,.T.);
#1437=ADVANCED_FACE('',(#246,#127),#161,.T.);
#1438=ADVANCED_FACE('',(#247),#105,.T.);
#1439=ADVANCED_FACE('',(#248),#1373,.T.);
#1440=ADVANCED_FACE('',(#249,#128),#162,.F.);
#1441=ADVANCED_FACE('',(#250),#1374,.F.);
#1442=ADVANCED_FACE('',(#251),#45,.F.);
#1481=CLOSED_SHELL('',(#1427,#1428,#1429,#1430,#1431,#1432));
#1482=CLOSED_SHELL('',(#1433,#1434,#1435,#1436,#1437,#1438,#1439,#1440,
#1441,#1442));
#1672=AXIS2_PLACEMENT_3D('',#2433,#1994,#1995);
#1673=AXIS2_PLACEMENT_3D('',#2434,#1996,#1997);
#1674=AXIS2_PLACEMENT_3D('',#2436,#1998,#1999);
#1675=AXIS2_PLACEMENT_3D('',#2438,#2000,#2001);
#1676=AXIS2_PLACEMENT_3D('',#2439,#2002,#2003);
#1677=AXIS2_PLACEMENT_3D('',#2441,#2004,#2005);
#1678=AXIS2_PLACEMENT_3D('',#2443,#2007,#2008);
#1679=AXIS2_PLACEMENT_3D('',#2446,#2010,#2011);
#1680=AXIS2_PLACEMENT_3D('',#2447,#2012,#2013);
#1681=AXIS2_PLACEMENT_3D('',#2450,#2015,#2016);
#1682=AXIS2_PLACEMENT_3D('',#2451,#2017,#2018);
#1683=AXIS2_PLACEMENT_3D('',#2453,#2019,#2020);
#1684=AXIS2_PLACEMENT_3D('',#2454,#2021,#2022);
#1685=AXIS2_PLACEMENT_3D('',#2456,#2024,#2025);
#1686=AXIS2_PLACEMENT_3D('',#2458,#2026,#2027);
#1687=AXIS2_PLACEMENT_3D('',#2460,#2028,#2029);
#1688=AXIS2_PLACEMENT_3D('',#2461,#2030,#2031);
#1689=AXIS2_PLACEMENT_3D('',#2464,#2033,#2034);
#1690=AXIS2_PLACEMENT_3D('',#2465,#2035,#2036);
#1691=AXIS2_PLACEMENT_3D('',#2467,#2037,#2038);
#1692=AXIS2_PLACEMENT_3D('',#2468,#2039,#2040);
#1693=AXIS2_PLACEMENT_3D('',#2470,#2041,#2042);
#1694=AXIS2_PLACEMENT_3D('',#2472,#2044,#2045);
#1695=AXIS2_PLACEMENT_3D('',#2474,#2046,#2047);
#1696=AXIS2_PLACEMENT_3D('',#2475,#2048,#2049);
#1697=AXIS2_PLACEMENT_3D('',#2477,#2050,#2051);
#1698=AXIS2_PLACEMENT_3D('',#2479,#2053,#2054);
#1699=AXIS2_PLACEMENT_3D('',#2482,#2056,#2057);
#1700=AXIS2_PLACEMENT_3D('',#2483,#2058,#2059);
#1701=AXIS2_PLACEMENT_3D('',#2485,#2060,#2061);
#1702=AXIS2_PLACEMENT_3D('',#2486,#2062,#2063);
#1703=AXIS2_PLACEMENT_3D('',#2488,#2065,#2066);
#1704=AXIS2_PLACEMENT_3D('',#2490,#2067,#2068);
#1994=DIRECTION('axis',(0.,0.,1.));
#1995=DIRECTION('refdir',(1.,0.,0.));
#1996=DIRECTION('center_axis',(0.,0.,1.));
#1997=DIRECTION('ref_axis',(-1.,0.,0.));
#1998=DIRECTION('center_axis',(0.,0.,-1.));
#1999=DIRECTION('ref_axis',(-1.,0.,0.));
#2000=DIRECTION('center_axis',(0.,0.,1.));
#2001=DIRECTION('ref_axis',(-1.,0.,0.));
#2002=DIRECTION('center_axis',(0.,0.,-1.));
#2003=DIRECTION('ref_axis',(-1.,0.,0.));
#2004=DIRECTION('center_axis',(0.,0.,-1.));
#2005=DIRECTION('ref_axis',(-1.,0.,0.));
#2006=DIRECTION('',(0.,0.,-1.));
#2007=DIRECTION('center_axis',(0.,0.,1.));
#2008=DIRECTION('ref_axis',(-1.,0.,0.));
#2009=DIRECTION('',(0.707106781186547,8.65956056235493E-17,0.707106781186548));
#2010=DIRECTION('center_axis',(0.,0.,1.));
#2011=DIRECTION('ref_axis',(-1.,0.,0.));
#2012=DIRECTION('center_axis',(0.,0.,-1.));
#2013=DIRECTION('ref_axis',(-1.,0.,0.));
#2014=DIRECTION('',(0.,0.,1.));
#2015=DIRECTION('center_axis',(0.,0.,1.));
#2016=DIRECTION('ref_axis',(-1.,0.,0.));
#2017=DIRECTION('center_axis',(0.,0.,1.));
#2018=DIRECTION('ref_axis',(-1.,0.,0.));
#2019=DIRECTION('center_axis',(0.,0.,-1.));
#2020=DIRECTION('ref_axis',(-1.,0.,0.));
#2021=DIRECTION('center_axis',(0.,0.,-1.));
#2022=DIRECTION('ref_axis',(-1.,0.,0.));
#2023=DIRECTION('',(-0.707106781186547,8.65956056235493E-17,0.707106781186548));
#2024=DIRECTION('center_axis',(0.,0.,1.));
#2025=DIRECTION('ref_axis',(-1.,0.,0.));
#2026=DIRECTION('center_axis',(0.,0.,-1.));
#2027=DIRECTION('ref_axis',(-1.,0.,0.));
#2028=DIRECTION('center_axis',(0.,0.,1.));
#2029=DIRECTION('ref_axis',(0.,-1.,0.));
#2030=DIRECTION('center_axis',(0.,0.,-1.));
#2031=DIRECTION('ref_axis',(-1.,0.,0.));
#2032=DIRECTION('',(0.,0.,1.));
#2033=DIRECTION('center_axis',(0.,0.,-1.));
#2034=DIRECTION('ref_axis',(-1.,0.,0.));
#2035=DIRECTION('center_axis',(0.,0.,1.));
#2036=DIRECTION('ref_axis',(-1.,0.,0.));
#2037=DIRECTION('center_axis',(0.,0.,1.));
#2038=DIRECTION('ref_axis',(-1.,0.,0.));
#2039=DIRECTION('center_axis',(0.,0.,-1.));
#2040=DIRECTION('ref_axis',(-1.,0.,0.));
#2041=DIRECTION('center_axis',(0.,0.,1.));
#2042=DIRECTION('ref_axis',(-1.,0.,0.));
#2043=DIRECTION('',(0.,0.,1.));
#2044=DIRECTION('center_axis',(0.,0.,1.));
#2045=DIRECTION('ref_axis',(-1.,0.,0.));
#2046=DIRECTION('center_axis',(0.,0.,-1.));
#2047=DIRECTION('ref_axis',(-1.,0.,0.));
#2048=DIRECTION('center_axis',(0.,0.,-1.));
#2049=DIRECTION('ref_axis',(-1.,0.,0.));
#2050=DIRECTION('center_axis',(0.,0.,-1.));
#2051=DIRECTION('ref_axis',(-1.,0.,0.));
#2052=DIRECTION('',(0.,0.,1.));
#2053=DIRECTION('center_axis',(0.,0.,1.));
#2054=DIRECTION('ref_axis',(-1.,0.,0.));
#2055=DIRECTION('',(-0.707106781186547,-8.65956056235493E-17,-0.707106781186548));
#2056=DIRECTION('center_axis',(0.,0.,1.));
#2057=DIRECTION('ref_axis',(-1.,0.,0.));
#2058=DIRECTION('center_axis',(0.,0.,1.));
#2059=DIRECTION('ref_axis',(-1.,0.,0.));
#2060=DIRECTION('center_axis',(0.,0.,-1.));
#2061=DIRECTION('ref_axis',(-1.,0.,0.));
#2062=DIRECTION('center_axis',(0.,0.,-1.));
#2063=DIRECTION('ref_axis',(-1.,0.,0.));
#2064=DIRECTION('',(0.707106781186547,-8.65956056235493E-17,-0.707106781186548));
#2065=DIRECTION('center_axis',(0.,0.,1.));
#2066=DIRECTION('ref_axis',(1.,0.,0.));
#2067=DIRECTION('center_axis',(0.,1.,0.));
#2068=DIRECTION('ref_axis',(-1.,0.,0.));
#2433=CARTESIAN_POINT('',(0.,0.,0.));
#2434=CARTESIAN_POINT('Origin',(-8.,-7.5,10.5));
#2435=CARTESIAN_POINT('',(-6.,-7.5,10.5));
#2436=CARTESIAN_POINT('Origin',(-8.,-7.5,10.5));
#2437=CARTESIAN_POINT('',(-7.,-7.5,10.5));
#2438=CARTESIAN_POINT('Origin',(-8.,-7.5,10.5));
#2439=CARTESIAN_POINT('Origin',(-8.,-7.5,12.5));
#2440=CARTESIAN_POINT('',(-7.,-7.5,12.3));
#2441=CARTESIAN_POINT('Origin',(-8.,-7.5,12.3));
#2442=CARTESIAN_POINT('',(-7.,-7.5,12.5));
#2443=CARTESIAN_POINT('Origin',(-8.,-7.5,12.4));
#2444=CARTESIAN_POINT('',(-6.8,-7.5,12.5));
#2445=CARTESIAN_POINT('',(-6.9,-7.5,12.4));
#2446=CARTESIAN_POINT('Origin',(-8.,-7.5,12.5));
#2447=CARTESIAN_POINT('Origin',(-8.,-7.5,12.5));
#2448=CARTESIAN_POINT('',(-6.,-7.5,12.3));
#2449=CARTESIAN_POINT('',(-6.,-7.5,12.5));
#2450=CARTESIAN_POINT('Origin',(-8.,-7.5,12.3));
#2451=CARTESIAN_POINT('Origin',(-8.,-7.5,12.5));
#2452=CARTESIAN_POINT('',(-6.2,-7.5,12.5));
#2453=CARTESIAN_POINT('Origin',(-8.,-7.5,12.5));
#2454=CARTESIAN_POINT('Origin',(-8.,-7.5,12.4));
#2455=CARTESIAN_POINT('',(-6.1,-7.5,12.4));
#2456=CARTESIAN_POINT('Origin',(-8.,-7.5,4.5));
#2457=CARTESIAN_POINT('',(-7.,-7.5,4.5));
#2458=CARTESIAN_POINT('Origin',(-8.,-7.5,4.5));
#2459=CARTESIAN_POINT('',(-8.86602540378444,-7.5,4.5));
#2460=CARTESIAN_POINT('Origin',(-8.,-7.5,4.5));
#2461=CARTESIAN_POINT('Origin',(-8.,-7.5,12.5));
#2462=CARTESIAN_POINT('',(-7.,-7.5,6.7));
#2463=CARTESIAN_POINT('',(-7.,-7.5,12.5));
#2464=CARTESIAN_POINT('Origin',(-8.,-7.5,6.7));
#2465=CARTESIAN_POINT('Origin',(-8.,-7.5,10.5));
#2466=CARTESIAN_POINT('',(-7.,-7.5,10.5));
#2467=CARTESIAN_POINT('Origin',(-8.,-7.5,10.5));
#2468=CARTESIAN_POINT('Origin',(-8.,-7.5,12.5));
#2469=CARTESIAN_POINT('',(-7.,-7.5,7.5));
#2470=CARTESIAN_POINT('Origin',(-8.,-7.5,7.5));
#2471=CARTESIAN_POINT('',(-7.,-7.5,12.5));
#2472=CARTESIAN_POINT('Origin',(-8.,-7.5,7.5));
#2473=CARTESIAN_POINT('',(-6.,-7.5,7.5));
#2474=CARTESIAN_POINT('Origin',(-8.,-7.5,7.5));
#2475=CARTESIAN_POINT('Origin',(-8.,-7.5,12.5));
#2476=CARTESIAN_POINT('',(-6.,-7.5,6.7));
#2477=CARTESIAN_POINT('Origin',(-8.,-7.5,6.7));
#2478=CARTESIAN_POINT('',(-6.,-7.5,12.5));
#2479=CARTESIAN_POINT('Origin',(-8.,-7.5,6.6));
#2480=CARTESIAN_POINT('',(-6.2,-7.5,6.5));
#2481=CARTESIAN_POINT('',(-6.1,-7.5,6.6));
#2482=CARTESIAN_POINT('Origin',(-8.,-7.5,6.5));
#2483=CARTESIAN_POINT('Origin',(-8.,-7.5,6.5));
#2484=CARTESIAN_POINT('',(-6.8,-7.5,6.5));
#2485=CARTESIAN_POINT('Origin',(-8.,-7.5,6.5));
#2486=CARTESIAN_POINT('Origin',(-8.,-7.5,6.6));
#2487=CARTESIAN_POINT('',(-6.9,-7.5,6.6));
#2488=CARTESIAN_POINT('Origin',(-8.,-7.5,4.));
#2489=CARTESIAN_POINT('',(-8.,-7.5,5.));
#2490=CARTESIAN_POINT('Origin',(-8.,-7.5,4.));
#2661=UNCERTAINTY_MEASURE_WITH_UNIT(LENGTH_MEASURE(0.01),#2677,
'DISTANCE_ACCURACY_VALUE',
'Maximum model space distance between geometric entities at asserted c
onnectivities');
#2666=UNCERTAINTY_MEASURE_WITH_UNIT(LENGTH_MEASURE(0.01),#2677,
'DISTANCE_ACCURACY_VALUE',
'Maximum model space distance between geometric entities at asserted c
onnectivities');
#2671=(
GEOMETRIC_REPRESENTATION_CONTEXT(3)
GLOBAL_UNCERTAINTY_ASSIGNED_CONTEXT((#2661))
GLOBAL_UNIT_ASSIGNED_CONTEXT((#2677,#2679,#2680))
REPRESENTATION_CONTEXT('','3D')
);
#2676=(
GEOMETRIC_REPRESENTATION_CONTEXT(3)
GLOBAL_UNCERTAINTY_ASSIGNED_CONTEXT((#2666))
GLOBAL_UNIT_ASSIGNED_CONTEXT((#2677,#2679,#2680))
REPRESENTATION_CONTEXT('','3D')
);
#2677=(
LENGTH_UNIT()
NAMED_UNIT(*)
SI_UNIT(.MILLI.,.METRE.)
);
#2679=(
NAMED_UNIT(*)
PLANE_ANGLE_UNIT()
SI_UNIT($,.RADIAN.)
);
#2680=(
NAMED_UNIT(*)
SI_UNIT($,.STERADIAN.)
SOLID_ANGLE_UNIT()
);
#2685=SHAPE_DEFINITION_REPRESENTATION(#2694,#2711);
#2694=PRODUCT_DEFINITION_SHAPE('',$,#2721);
#2711=SHAPE_REPRESENTATION('',(#1672),#2671);
#2716=PRODUCT_DEFINITION_CONTEXT('part definition',#2745,'design');
#2721=PRODUCT_DEFINITION('Screw_03','Screw_03',#2730,#2716);
#2730=PRODUCT_DEFINITION_FORMATION('',$,#2751);
#2745=APPLICATION_CONTEXT(
'Core Data for Automotive Mechanical Design Process');
#2746=PRODUCT_CONTEXT('part definition',#2745,'mechanical');
#2751=PRODUCT('Screw_03','Screw_03',$,(#2746));
#2757=PRESENTATION_STYLE_ASSIGNMENT((#2759));
#2759=SURFACE_STYLE_USAGE(.BOTH.,#2761);
#2761=SURFACE_SIDE_STYLE('',(#2763));
#2763=SURFACE_STYLE_FILL_AREA(#2765);
#2765=FILL_AREA_STYLE('Opaque(203,203,203)',(#2767));
#2767=FILL_AREA_STYLE_COLOUR('Opaque(203,203,203)',#2769);
#2769=COLOUR_RGB('Opaque(203,203,203)', 0.09019608, 0.27058824, 0.51372549);
ENDSEC;
END-ISO-10303-21;
